ISO-10303-21;
HEADER;
/* Generated by software containing ST-Developer
 * from STEP Tools, Inc. (www.steptools.com) 
 */

FILE_DESCRIPTION(
/* description */ ('Bell-crank linkage with push rods'),
/* implementation_level */ '2;1');

FILE_NAME(
/* name */ 'M4x10 Cap Screw.step',
/* time_stamp */ '2026-10-28T03:25:15-07:00',
/* author */ (''),
/* organization */ (''),
/* preprocessor_version */ 'ST-DEVELOPER v20.2',
/* originating_system */ 'Autodesk Translation Framework v15.17.0.0',
/* authorisation */ '');

FILE_SCHEMA (('AUTOMOTIVE_DESIGN { 1 0 10303 214 3 1 1 }'));
ENDSEC;

DATA;
#10=MECHANICAL_DESIGN_GEOMETRIC_PRESENTATION_REPRESENTATION('',(#665),#16678);
#448=CONICAL_SURFACE('',#10531,0.325,0.785398163397448);
#449=CONICAL_SURFACE('',#10535,0.335,0.785398163397448);
#450=CONICAL_SURFACE('',#10539,0.21,0.463647609000806);
#453=ORIENTED_CLOSED_SHELL('',*,#8857,.F.);
#456=BREP_WITH_VOIDS('Body1',#8858,(#453));
#549=SHAPE_REPRESENTATION_RELATIONSHIP('SRR','None',#16972,#603);
#603=ADVANCED_BREP_SHAPE_REPRESENTATION('',(#456),#16677);
#665=STYLED_ITEM('',(#17298),#456);
#965=FACE_BOUND('',#2529,.T.);
#1236=PLANE('',#10519);
#1237=PLANE('',#10520);
#1238=PLANE('',#10521);
#1239=PLANE('',#10522);
#1240=PLANE('',#10523);
#1241=PLANE('',#10524);
#1242=PLANE('',#10525);
#1243=PLANE('',#10526);
#1244=PLANE('',#10527);
#1245=PLANE('',#10529);
#1246=PLANE('',#10537);
#1753=FACE_OUTER_BOUND('',#2515,.T.);
#1754=FACE_OUTER_BOUND('',#2516,.T.);
#1755=FACE_OUTER_BOUND('',#2517,.T.);
#1756=FACE_OUTER_BOUND('',#2518,.T.);
#1757=FACE_OUTER_BOUND('',#2519,.T.);
#1758=FACE_OUTER_BOUND('',#2520,.T.);
#1759=FACE_OUTER_BOUND('',#2521,.T.);
#1760=FACE_OUTER_BOUND('',#2522,.T.);
#1761=FACE_OUTER_BOUND('',#2523,.T.);
#1762=FACE_OUTER_BOUND('',#2524,.T.);
#1763=FACE_OUTER_BOUND('',#2525,.T.);
#1764=FACE_OUTER_BOUND('',#2526,.T.);
#1765=FACE_OUTER_BOUND('',#2527,.T.);
#1766=FACE_OUTER_BOUND('',#2528,.T.);
#1767=FACE_OUTER_BOUND('',#2530,.T.);
#1768=FACE_OUTER_BOUND('',#2531,.T.);
#2515=EDGE_LOOP('',(#8007,#8008,#8009,#8010));
#2516=EDGE_LOOP('',(#8011,#8012,#8013,#8014));
#2517=EDGE_LOOP('',(#8015,#8016,#8017,#8018));
#2518=EDGE_LOOP('',(#8019,#8020,#8021,#8022));
#2519=EDGE_LOOP('',(#8023,#8024,#8025,#8026));
#2520=EDGE_LOOP('',(#8027,#8028,#8029,#8030));
#2521=EDGE_LOOP('',(#8031,#8032,#8033,#8034,#8035,#8036));
#2522=EDGE_LOOP('',(#8037,#8038,#8039,#8040,#8041,#8042));
#2523=EDGE_LOOP('',(#8043));
#2524=EDGE_LOOP('',(#8044));
#2525=EDGE_LOOP('',(#8045,#8046,#8047,#8048));
#2526=EDGE_LOOP('',(#8049,#8050,#8051,#8052));
#2527=EDGE_LOOP('',(#8053,#8054,#8055,#8056));
#2528=EDGE_LOOP('',(#8057));
#2529=EDGE_LOOP('',(#8058));
#2530=EDGE_LOOP('',(#8059,#8060,#8061,#8062));
#2531=EDGE_LOOP('',(#8063,#8064,#8065,#8066));
#3058=LINE('',#16401,#3607);
#3059=LINE('',#16403,#3608);
#3060=LINE('',#16405,#3609);
#3061=LINE('',#16406,#3610);
#3062=LINE('',#16409,#3611);
#3063=LINE('',#16411,#3612);
#3064=LINE('',#16412,#3613);
#3065=LINE('',#16415,#3614);
#3066=LINE('',#16417,#3615);
#3067=LINE('',#16418,#3616);
#3068=LINE('',#16421,#3617);
#3069=LINE('',#16423,#3618);
#3070=LINE('',#16424,#3619);
#3071=LINE('',#16427,#3620);
#3072=LINE('',#16429,#3621);
#3073=LINE('',#16430,#3622);
#3074=LINE('',#16432,#3623);
#3075=LINE('',#16433,#3624);
#3076=LINE('',#16445,#3625);
#3077=LINE('',#16449,#3626);
#3078=LINE('',#16453,#3627);
#3079=LINE('',#16460,#3628);
#3080=LINE('',#16462,#3629);
#3607=VECTOR('',#13288,1.);
#3608=VECTOR('',#13289,1.);
#3609=VECTOR('',#13290,1.);
#3610=VECTOR('',#13291,1.);
#3611=VECTOR('',#13294,1.);
#3612=VECTOR('',#13295,1.);
#3613=VECTOR('',#13296,1.);
#3614=VECTOR('',#13299,1.);
#3615=VECTOR('',#13300,1.);
#3616=VECTOR('',#13301,1.);
#3617=VECTOR('',#13304,1.);
#3618=VECTOR('',#13305,1.);
#3619=VECTOR('',#13306,1.);
#3620=VECTOR('',#13309,1.);
#3621=VECTOR('',#13310,1.);
#3622=VECTOR('',#13311,1.);
#3623=VECTOR('',#13314,1.);
#3624=VECTOR('',#13315,1.);
#3625=VECTOR('',#13332,0.325);
#3626=VECTOR('',#13337,0.35);
#3627=VECTOR('',#13342,0.335);
#3628=VECTOR('',#13351,0.21);
#3629=VECTOR('',#13354,0.2);
#4113=CIRCLE('',#10528,0.1954);
#4114=CIRCLE('',#10530,0.3);
#4115=CIRCLE('',#10532,0.35);
#4116=CIRCLE('',#10534,0.35);
#4117=CIRCLE('',#10536,0.32);
#4118=CIRCLE('',#10538,0.22);
#4119=CIRCLE('',#10540,0.1954);
#4814=VERTEX_POINT('',#16399);
#4815=VERTEX_POINT('',#16400);
#4816=VERTEX_POINT('',#16402);
#4817=VERTEX_POINT('',#16404);
#4818=VERTEX_POINT('',#16408);
#4819=VERTEX_POINT('',#16410);
#4820=VERTEX_POINT('',#16414);
#4821=VERTEX_POINT('',#16416);
#4822=VERTEX_POINT('',#16420);
#4823=VERTEX_POINT('',#16422);
#4824=VERTEX_POINT('',#16426);
#4825=VERTEX_POINT('',#16428);
#4826=VERTEX_POINT('',#16437);
#4827=VERTEX_POINT('',#16440);
#4828=VERTEX_POINT('',#16443);
#4829=VERTEX_POINT('',#16447);
#4830=VERTEX_POINT('',#16451);
#4831=VERTEX_POINT('',#16455);
#4832=VERTEX_POINT('',#16458);
#5881=EDGE_CURVE('',#4814,#4815,#3058,.T.);
#5882=EDGE_CURVE('',#4815,#4816,#3059,.T.);
#5883=EDGE_CURVE('',#4816,#4817,#3060,.T.);
#5884=EDGE_CURVE('',#4814,#4817,#3061,.T.);
#5885=EDGE_CURVE('',#4815,#4818,#3062,.T.);
#5886=EDGE_CURVE('',#4818,#4819,#3063,.T.);
#5887=EDGE_CURVE('',#4819,#4816,#3064,.T.);
#5888=EDGE_CURVE('',#4818,#4820,#3065,.T.);
#5889=EDGE_CURVE('',#4820,#4821,#3066,.T.);
#5890=EDGE_CURVE('',#4821,#4819,#3067,.T.);
#5891=EDGE_CURVE('',#4820,#4822,#3068,.T.);
#5892=EDGE_CURVE('',#4822,#4823,#3069,.T.);
#5893=EDGE_CURVE('',#4823,#4821,#3070,.T.);
#5894=EDGE_CURVE('',#4822,#4824,#3071,.T.);
#5895=EDGE_CURVE('',#4824,#4825,#3072,.T.);
#5896=EDGE_CURVE('',#4825,#4823,#3073,.T.);
#5897=EDGE_CURVE('',#4824,#4814,#3074,.T.);
#5898=EDGE_CURVE('',#4817,#4825,#3075,.T.);
#5899=EDGE_CURVE('',#4826,#4826,#4113,.T.);
#5900=EDGE_CURVE('',#4827,#4827,#4114,.T.);
#5901=EDGE_CURVE('',#4828,#4828,#4115,.T.);
#5902=EDGE_CURVE('',#4828,#4827,#3076,.T.);
#5903=EDGE_CURVE('',#4829,#4829,#4116,.T.);
#5904=EDGE_CURVE('',#4829,#4828,#3077,.T.);
#5905=EDGE_CURVE('',#4830,#4830,#4117,.T.);
#5906=EDGE_CURVE('',#4830,#4829,#3078,.T.);
#5907=EDGE_CURVE('',#4831,#4831,#4118,.T.);
#5908=EDGE_CURVE('',#4832,#4832,#4119,.F.);
#5909=EDGE_CURVE('',#4832,#4831,#3079,.T.);
#5910=EDGE_CURVE('',#4826,#4832,#3080,.T.);
#8007=ORIENTED_EDGE('',*,*,#5881,.T.);
#8008=ORIENTED_EDGE('',*,*,#5882,.T.);
#8009=ORIENTED_EDGE('',*,*,#5883,.T.);
#8010=ORIENTED_EDGE('',*,*,#5884,.F.);
#8011=ORIENTED_EDGE('',*,*,#5885,.T.);
#8012=ORIENTED_EDGE('',*,*,#5886,.T.);
#8013=ORIENTED_EDGE('',*,*,#5887,.T.);
#8014=ORIENTED_EDGE('',*,*,#5882,.F.);
#8015=ORIENTED_EDGE('',*,*,#5888,.T.);
#8016=ORIENTED_EDGE('',*,*,#5889,.T.);
#8017=ORIENTED_EDGE('',*,*,#5890,.T.);
#8018=ORIENTED_EDGE('',*,*,#5886,.F.);
#8019=ORIENTED_EDGE('',*,*,#5891,.T.);
#8020=ORIENTED_EDGE('',*,*,#5892,.T.);
#8021=ORIENTED_EDGE('',*,*,#5893,.T.);
#8022=ORIENTED_EDGE('',*,*,#5889,.F.);
#8023=ORIENTED_EDGE('',*,*,#5894,.T.);
#8024=ORIENTED_EDGE('',*,*,#5895,.T.);
#8025=ORIENTED_EDGE('',*,*,#5896,.T.);
#8026=ORIENTED_EDGE('',*,*,#5892,.F.);
#8027=ORIENTED_EDGE('',*,*,#5897,.T.);
#8028=ORIENTED_EDGE('',*,*,#5884,.T.);
#8029=ORIENTED_EDGE('',*,*,#5898,.T.);
#8030=ORIENTED_EDGE('',*,*,#5895,.F.);
#8031=ORIENTED_EDGE('',*,*,#5897,.F.);
#8032=ORIENTED_EDGE('',*,*,#5894,.F.);
#8033=ORIENTED_EDGE('',*,*,#5891,.F.);
#8034=ORIENTED_EDGE('',*,*,#5888,.F.);
#8035=ORIENTED_EDGE('',*,*,#5885,.F.);
#8036=ORIENTED_EDGE('',*,*,#5881,.F.);
#8037=ORIENTED_EDGE('',*,*,#5898,.F.);
#8038=ORIENTED_EDGE('',*,*,#5883,.F.);
#8039=ORIENTED_EDGE('',*,*,#5887,.F.);
#8040=ORIENTED_EDGE('',*,*,#5890,.F.);
#8041=ORIENTED_EDGE('',*,*,#5893,.F.);
#8042=ORIENTED_EDGE('',*,*,#5896,.F.);
#8043=ORIENTED_EDGE('',*,*,#5899,.F.);
#8044=ORIENTED_EDGE('',*,*,#5900,.F.);
#8045=ORIENTED_EDGE('',*,*,#5901,.F.);
#8046=ORIENTED_EDGE('',*,*,#5902,.T.);
#8047=ORIENTED_EDGE('',*,*,#5900,.T.);
#8048=ORIENTED_EDGE('',*,*,#5902,.F.);
#8049=ORIENTED_EDGE('',*,*,#5903,.F.);
#8050=ORIENTED_EDGE('',*,*,#5904,.T.);
#8051=ORIENTED_EDGE('',*,*,#5901,.T.);
#8052=ORIENTED_EDGE('',*,*,#5904,.F.);
#8053=ORIENTED_EDGE('',*,*,#5905,.F.);
#8054=ORIENTED_EDGE('',*,*,#5906,.T.);
#8055=ORIENTED_EDGE('',*,*,#5903,.T.);
#8056=ORIENTED_EDGE('',*,*,#5906,.F.);
#8057=ORIENTED_EDGE('',*,*,#5905,.T.);
#8058=ORIENTED_EDGE('',*,*,#5907,.F.);
#8059=ORIENTED_EDGE('',*,*,#5908,.F.);
#8060=ORIENTED_EDGE('',*,*,#5909,.T.);
#8061=ORIENTED_EDGE('',*,*,#5907,.T.);
#8062=ORIENTED_EDGE('',*,*,#5909,.F.);
#8063=ORIENTED_EDGE('',*,*,#5899,.T.);
#8064=ORIENTED_EDGE('',*,*,#5910,.T.);
#8065=ORIENTED_EDGE('',*,*,#5908,.T.);
#8066=ORIENTED_EDGE('',*,*,#5910,.F.);
#8270=CYLINDRICAL_SURFACE('',#10533,0.35);
#8271=CYLINDRICAL_SURFACE('',#10541,0.1954);
#8778=ADVANCED_FACE('',(#1753),#1236,.F.);
#8779=ADVANCED_FACE('',(#1754),#1237,.F.);
#8780=ADVANCED_FACE('',(#1755),#1238,.F.);
#8781=ADVANCED_FACE('',(#1756),#1239,.F.);
#8782=ADVANCED_FACE('',(#1757),#1240,.F.);
#8783=ADVANCED_FACE('',(#1758),#1241,.F.);
#8784=ADVANCED_FACE('',(#1759),#1242,.F.);
#8785=ADVANCED_FACE('',(#1760),#1243,.F.);
#8786=ADVANCED_FACE('',(#1761),#1244,.F.);
#8787=ADVANCED_FACE('',(#1762),#1245,.T.);
#8788=ADVANCED_FACE('',(#1763),#448,.T.);
#8789=ADVANCED_FACE('',(#1764),#8270,.T.);
#8790=ADVANCED_FACE('',(#1765),#449,.T.);
#8791=ADVANCED_FACE('',(#1766,#965),#1246,.T.);
#8792=ADVANCED_FACE('',(#1767),#450,.T.);
#8793=ADVANCED_FACE('',(#1768),#8271,.T.);
#8857=CLOSED_SHELL('',(#8778,#8779,#8780,#8781,#8782,#8783,#8784,#8785));
#8858=CLOSED_SHELL('',(#8786,#8787,#8788,#8789,#8790,#8791,#8792,#8793));
#10518=AXIS2_PLACEMENT_3D('',#16397,#13284,#13285);
#10519=AXIS2_PLACEMENT_3D('',#16398,#13286,#13287);
#10520=AXIS2_PLACEMENT_3D('',#16407,#13292,#13293);
#10521=AXIS2_PLACEMENT_3D('',#16413,#13297,#13298);
#10522=AXIS2_PLACEMENT_3D('',#16419,#13302,#13303);
#10523=AXIS2_PLACEMENT_3D('',#16425,#13307,#13308);
#10524=AXIS2_PLACEMENT_3D('',#16431,#13312,#13313);
#10525=AXIS2_PLACEMENT_3D('',#16434,#13316,#13317);
#10526=AXIS2_PLACEMENT_3D('',#16435,#13318,#13319);
#10527=AXIS2_PLACEMENT_3D('',#16436,#13320,#13321);
#10528=AXIS2_PLACEMENT_3D('',#16438,#13322,#13323);
#10529=AXIS2_PLACEMENT_3D('',#16439,#13324,#13325);
#10530=AXIS2_PLACEMENT_3D('',#16441,#13326,#13327);
#10531=AXIS2_PLACEMENT_3D('',#16442,#13328,#13329);
#10532=AXIS2_PLACEMENT_3D('',#16444,#13330,#13331);
#10533=AXIS2_PLACEMENT_3D('',#16446,#13333,#13334);
#10534=AXIS2_PLACEMENT_3D('',#16448,#13335,#13336);
#10535=AXIS2_PLACEMENT_3D('',#16450,#13338,#13339);
#10536=AXIS2_PLACEMENT_3D('',#16452,#13340,#13341);
#10537=AXIS2_PLACEMENT_3D('',#16454,#13343,#13344);
#10538=AXIS2_PLACEMENT_3D('',#16456,#13345,#13346);
#10539=AXIS2_PLACEMENT_3D('',#16457,#13347,#13348);
#10540=AXIS2_PLACEMENT_3D('',#16459,#13349,#13350);
#10541=AXIS2_PLACEMENT_3D('',#16461,#13352,#13353);
#13284=DIRECTION('axis',(0.,0.,1.));
#13285=DIRECTION('refdir',(1.,0.,0.));
#13286=DIRECTION('center_axis',(0.866025403784439,0.,-0.5));
#13287=DIRECTION('ref_axis',(0.5,0.,0.866025403784439));
#13288=DIRECTION('',(-0.5,0.,-0.866025403784439));
#13289=DIRECTION('',(0.,-1.,0.));
#13290=DIRECTION('',(0.5,0.,0.866025403784439));
#13291=DIRECTION('',(0.,-1.,0.));
#13292=DIRECTION('center_axis',(1.60246890531964E-16,0.,-1.));
#13293=DIRECTION('ref_axis',(1.,0.,1.60246890531964E-16));
#13294=DIRECTION('',(-1.,0.,-1.60246890531964E-16));
#13295=DIRECTION('',(0.,-1.,0.));
#13296=DIRECTION('',(1.,0.,1.60246890531964E-16));
#13297=DIRECTION('center_axis',(-0.866025403784439,0.,-0.5));
#13298=DIRECTION('ref_axis',(0.5,0.,-0.866025403784439));
#13299=DIRECTION('',(-0.5,0.,0.866025403784439));
#13300=DIRECTION('',(0.,-1.,0.));
#13301=DIRECTION('',(0.5,0.,-0.866025403784439));
#13302=DIRECTION('center_axis',(-0.866025403784439,0.,0.5));
#13303=DIRECTION('ref_axis',(-0.5,0.,-0.866025403784439));
#13304=DIRECTION('',(0.5,0.,0.866025403784439));
#13305=DIRECTION('',(0.,-1.,0.));
#13306=DIRECTION('',(-0.5,0.,-0.866025403784439));
#13307=DIRECTION('center_axis',(-1.60246890531964E-16,0.,1.));
#13308=DIRECTION('ref_axis',(-1.,0.,-1.60246890531964E-16));
#13309=DIRECTION('',(1.,0.,1.60246890531964E-16));
#13310=DIRECTION('',(0.,-1.,0.));
#13311=DIRECTION('',(-1.,0.,-1.60246890531964E-16));
#13312=DIRECTION('center_axis',(0.866025403784439,0.,0.5));
#13313=DIRECTION('ref_axis',(-0.5,0.,0.866025403784439));
#13314=DIRECTION('',(0.5,0.,-0.866025403784439));
#13315=DIRECTION('',(-0.5,0.,0.866025403784439));
#13316=DIRECTION('center_axis',(0.,1.,0.));
#13317=DIRECTION('ref_axis',(1.,0.,0.));
#13318=DIRECTION('center_axis',(0.,-1.,0.));
#13319=DIRECTION('ref_axis',(0.,0.,-1.));
#13320=DIRECTION('center_axis',(0.,1.,0.));
#13321=DIRECTION('ref_axis',(1.,0.,0.));
#13322=DIRECTION('center_axis',(0.,1.,0.));
#13323=DIRECTION('ref_axis',(1.,0.,0.));
#13324=DIRECTION('center_axis',(0.,1.,0.));
#13325=DIRECTION('ref_axis',(0.,0.,1.));
#13326=DIRECTION('center_axis',(0.,-1.,0.));
#13327=DIRECTION('ref_axis',(1.,0.,0.));
#13328=DIRECTION('center_axis',(0.,-1.,0.));
#13329=DIRECTION('ref_axis',(1.,0.,0.));
#13330=DIRECTION('center_axis',(0.,-1.,0.));
#13331=DIRECTION('ref_axis',(1.,0.,0.));
#13332=DIRECTION('',(0.707106781186547,0.707106781186548,8.65956056235493E-17));
#13333=DIRECTION('center_axis',(0.,-1.,0.));
#13334=DIRECTION('ref_axis',(1.,0.,0.));
#13335=DIRECTION('center_axis',(0.,-1.,0.));
#13336=DIRECTION('ref_axis',(1.,0.,0.));
#13337=DIRECTION('',(0.,1.,0.));
#13338=DIRECTION('center_axis',(0.,1.,0.));
#13339=DIRECTION('ref_axis',(1.,0.,0.));
#13340=DIRECTION('center_axis',(0.,-1.,0.));
#13341=DIRECTION('ref_axis',(1.,0.,0.));
#13342=DIRECTION('',(-0.707106781186547,0.707106781186548,-8.65956056235493E-17));
#13343=DIRECTION('center_axis',(0.,-1.,0.));
#13344=DIRECTION('ref_axis',(0.,0.,-1.));
#13345=DIRECTION('center_axis',(0.,-1.,0.));
#13346=DIRECTION('ref_axis',(1.,0.,0.));
#13347=DIRECTION('center_axis',(0.,1.,0.));
#13348=DIRECTION('ref_axis',(1.,0.,0.));
#13349=DIRECTION('center_axis',(0.,1.,0.));
#13350=DIRECTION('ref_axis',(1.,0.,0.));
#13351=DIRECTION('',(-0.447213595499958,0.894427190999916,-5.47678698264203E-17));
#13352=DIRECTION('center_axis',(0.,-1.,0.));
#13353=DIRECTION('ref_axis',(1.,0.,0.));
#13354=DIRECTION('',(0.,1.,0.));
#16397=CARTESIAN_POINT('',(0.,0.,0.));
#16398=CARTESIAN_POINT('Origin',(0.0866025403784439,-0.4,-0.15));
#16399=CARTESIAN_POINT('',(0.173205080756888,-0.4,0.));
#16400=CARTESIAN_POINT('',(0.0866025403784439,-0.4,-0.15));
#16401=CARTESIAN_POINT('',(0.173205080756888,-0.4,0.));
#16402=CARTESIAN_POINT('',(0.0866025403784439,-0.64,-0.15));
#16403=CARTESIAN_POINT('',(0.0866025403784439,-0.4,-0.15));
#16404=CARTESIAN_POINT('',(0.173205080756888,-0.64,0.));
#16405=CARTESIAN_POINT('',(0.173205080756888,-0.64,0.));
#16406=CARTESIAN_POINT('',(0.173205080756888,-0.4,0.));
#16407=CARTESIAN_POINT('Origin',(-0.0866025403784438,-0.4,-0.15));
#16408=CARTESIAN_POINT('',(-0.0866025403784438,-0.4,-0.15));
#16409=CARTESIAN_POINT('',(0.0866025403784439,-0.4,-0.15));
#16410=CARTESIAN_POINT('',(-0.0866025403784438,-0.64,-0.15));
#16411=CARTESIAN_POINT('',(-0.0866025403784438,-0.4,-0.15));
#16412=CARTESIAN_POINT('',(0.0866025403784439,-0.64,-0.15));
#16413=CARTESIAN_POINT('Origin',(-0.173205080756888,-0.4,-2.77555756156289E-17));
#16414=CARTESIAN_POINT('',(-0.173205080756888,-0.4,-2.12115047744981E-17));
#16415=CARTESIAN_POINT('',(-0.0866025403784438,-0.4,-0.15));
#16416=CARTESIAN_POINT('',(-0.173205080756888,-0.64,-2.77555756156289E-17));
#16417=CARTESIAN_POINT('',(-0.173205080756888,-0.4,-2.12115047744981E-17));
#16418=CARTESIAN_POINT('',(-0.0866025403784438,-0.64,-0.15));
#16419=CARTESIAN_POINT('Origin',(-0.0866025403784439,-0.4,0.15));
#16420=CARTESIAN_POINT('',(-0.0866025403784439,-0.4,0.15));
#16421=CARTESIAN_POINT('',(-0.173205080756888,-0.4,-2.12115047744981E-17));
#16422=CARTESIAN_POINT('',(-0.0866025403784439,-0.64,0.15));
#16423=CARTESIAN_POINT('',(-0.0866025403784439,-0.4,0.15));
#16424=CARTESIAN_POINT('',(-0.173205080756888,-0.64,-2.12115047744981E-17));
#16425=CARTESIAN_POINT('Origin',(0.0866025403784439,-0.4,0.15));
#16426=CARTESIAN_POINT('',(0.0866025403784439,-0.4,0.15));
#16427=CARTESIAN_POINT('',(-0.0866025403784439,-0.4,0.15));
#16428=CARTESIAN_POINT('',(0.0866025403784439,-0.64,0.15));
#16429=CARTESIAN_POINT('',(0.0866025403784439,-0.4,0.15));
#16430=CARTESIAN_POINT('',(-0.0866025403784439,-0.64,0.15));
#16431=CARTESIAN_POINT('Origin',(0.173205080756888,-0.4,0.));
#16432=CARTESIAN_POINT('',(0.0866025403784439,-0.4,0.15));
#16433=CARTESIAN_POINT('',(0.0866025403784439,-0.64,0.15));
#16434=CARTESIAN_POINT('Origin',(0.,-0.4,-2.77555756156289E-17));
#16435=CARTESIAN_POINT('Origin',(0.,-0.64,-2.77555756156289E-17));
#16436=CARTESIAN_POINT('Origin',(0.,-1.,0.));
#16437=CARTESIAN_POINT('',(-0.1954,-1.,2.39295984553393E-17));
#16438=CARTESIAN_POINT('Origin',(0.,-1.,0.));
#16439=CARTESIAN_POINT('Origin',(0.3,0.4,0.));
#16440=CARTESIAN_POINT('',(-0.3,0.4,-3.67394039744206E-17));
#16441=CARTESIAN_POINT('Origin',(0.,0.4,0.));
#16442=CARTESIAN_POINT('Origin',(0.,0.375,0.));
#16443=CARTESIAN_POINT('',(-0.35,0.35,-4.28626379701573E-17));
#16444=CARTESIAN_POINT('Origin',(0.,0.35,0.));
#16445=CARTESIAN_POINT('',(-0.325,0.375,-3.9801020972289E-17));
#16446=CARTESIAN_POINT('Origin',(0.,0.19,0.));
#16447=CARTESIAN_POINT('',(-0.35,0.03,-4.28626379701574E-17));
#16448=CARTESIAN_POINT('Origin',(0.,0.03,0.));
#16449=CARTESIAN_POINT('',(-0.35,0.19,-4.28626379701574E-17));
#16450=CARTESIAN_POINT('Origin',(0.,0.0149999999999999,0.));
#16451=CARTESIAN_POINT('',(-0.32,-3.29597460435593E-17,-3.91886975727153E-17));
#16452=CARTESIAN_POINT('Origin',(0.,0.,0.));
#16453=CARTESIAN_POINT('',(-0.335,0.0149999999999999,-4.10256677714363E-17));
#16454=CARTESIAN_POINT('Origin',(0.22,0.,0.));
#16455=CARTESIAN_POINT('',(-0.22,-6.93889390390723E-18,-2.69422295812418E-17));
#16456=CARTESIAN_POINT('Origin',(0.,0.,0.));
#16457=CARTESIAN_POINT('Origin',(0.,-0.02,0.));
#16458=CARTESIAN_POINT('',(-0.1954,-0.0492,2.39295984553393E-17));
#16459=CARTESIAN_POINT('Origin',(0.,-0.0492,0.));
#16460=CARTESIAN_POINT('',(-0.21,-0.02,-2.57175827820944E-17));
#16461=CARTESIAN_POINT('Origin',(0.,-0.8,0.));
#16462=CARTESIAN_POINT('',(-0.1954,-0.8,-2.39295984553393E-17));
#16613=UNCERTAINTY_MEASURE_WITH_UNIT(LENGTH_MEASURE(0.001),#16679,
'DISTANCE_ACCURACY_VALUE',
'Maximum model space distance between geometric entities at asserted c
onnectivities');
#16614=UNCERTAINTY_MEASURE_WITH_UNIT(LENGTH_MEASURE(0.001),#16679,
'DISTANCE_ACCURACY_VALUE',
'Maximum model space distance between geometric entities at asserted c
onnectivities');
#16677=(
GEOMETRIC_REPRESENTATION_CONTEXT(3)
GLOBAL_UNCERTAINTY_ASSIGNED_CONTEXT((#16613))
GLOBAL_UNIT_ASSIGNED_CONTEXT((#16679,#16681,#16682))
REPRESENTATION_CONTEXT('','3D')
);
#16678=(
GEOMETRIC_REPRESENTATION_CONTEXT(3)
GLOBAL_UNCERTAINTY_ASSIGNED_CONTEXT((#16614))
GLOBAL_UNIT_ASSIGNED_CONTEXT((#16679,#16681,#16682))
REPRESENTATION_CONTEXT('','3D')
);
#16679=(
LENGTH_UNIT()
NAMED_UNIT(*)
SI_UNIT(.CENTI.,.METRE.)
);
#16681=(
NAMED_UNIT(*)
PLANE_ANGLE_UNIT()
SI_UNIT($,.RADIAN.)
);
#16682=(
NAMED_UNIT(*)
SI_UNIT($,.STERADIAN.)
SOLID_ANGLE_UNIT()
);
#16745=SHAPE_DEFINITION_REPRESENTATION(#16821,#16972);
#16821=PRODUCT_DEFINITION_SHAPE('',$,#17036);
#16972=SHAPE_REPRESENTATION('',(#10518),#16677);
#16973=PRODUCT_DEFINITION_CONTEXT('part definition',#17164,'design');
#17036=PRODUCT_DEFINITION('M4x10 Cap Screw','M4x10 Cap Screw',#17099,#16973);
#17099=PRODUCT_DEFINITION_FORMATION('',$,#17228);
#17164=APPLICATION_CONTEXT(
'Core Data for Automotive Mechanical Design Process');
#17165=PRODUCT_CONTEXT('part definition',#17164,'mechanical');
#17228=PRODUCT('M4x10 Cap Screw','M4x10 Cap Screw','M4x10 Cap Screw',(#17165));
#17292=COLOUR_RGB('Black',0.12,0.14,0.17);
#17293=FILL_AREA_STYLE_COLOUR('',#17292);
#17294=FILL_AREA_STYLE('',(#17293));
#17295=SURFACE_STYLE_FILL_AREA(#17294);
#17296=SURFACE_SIDE_STYLE('',(#17295));
#17297=SURFACE_STYLE_USAGE(.BOTH.,#17296);
#17298=PRESENTATION_STYLE_ASSIGNMENT((#17297));
ENDSEC;
END-ISO-10303-21;
